ISO-10303-21;
HEADER;
FILE_DESCRIPTION (('STEP AP203'),
    '1' );
FILE_NAME ('1602p_c_04.step',
    '2026-10-31T14:11:27',
    ( '' ),
    ( '' ),
    'SwSTEP 2.0',
    'SolidWorks 2024',
    '' );
FILE_SCHEMA (( 'AUTOMOTIVE_DESIGN' ));
ENDSEC;

DATA;
#85=AXIS2_PLACEMENT_3D ( 'NONE', #8202, #22670, #2860 ) ;
#135=DIRECTION ( 'NONE',  ( -1.000000000000000000, 0.000000000000000000, 0.000000000000000000 ) ) ;
#181=ADVANCED_FACE ( 'NONE', ( #7395 ), #2255, .T. ) ;
#297=ORIENTED_EDGE ( 'NONE', *, *, #15434, .T. ) ;
#308=DIRECTION ( 'NONE',  ( -1.000000000000000000, 0.000000000000000000, 0.000000000000000000 ) ) ;
#316=CLOSED_SHELL ( 'NONE', ( #181, #9383, #7532, #3257, #22716, #15891 ) ) ;
#341=VERTEX_POINT ( 'NONE', #22760 ) ;
#415=DIRECTION ( 'NONE',  ( 1.000000000000000000, 0.000000000000000000, 0.000000000000000000 ) ) ;
#460=EDGE_LOOP ( 'NONE', ( #10662, #7754 ) ) ;
#703=ORIENTED_EDGE ( 'NONE', *, *, #8835, .F. ) ;
#732=FACE_OUTER_BOUND ( 'NONE', #3446, .T. ) ;
#765=DIRECTION ( 'NONE',  ( -1.000000000000000000, 0.000000000000000000, -3.099353312215989675E-62 ) ) ;
#987=DIRECTION ( 'NONE',  ( 3.099353312215988811E-62, -1.534091707905539548E-92, -1.000000000000000000 ) ) ;
#1217=EDGE_CURVE ( 'NONE', #2335, #2485, #7484, .T. ) ;
#1293=ORIENTED_EDGE ( 'NONE', *, *, #4934, .F. ) ;
#1316=CARTESIAN_POINT ( 'NONE',  ( -16.50000000000000000, -20.00000000000000000, 5.000000000000000000 ) ) ;
#1394=DIRECTION ( 'NONE',  ( 3.099353312215988811E-62, -1.534091707905539548E-92, -1.000000000000000000 ) ) ;
#1716=DIRECTION ( 'NONE',  ( 3.099353312215988811E-62, -1.534091707905539548E-92, -1.000000000000000000 ) ) ;
#1718=CARTESIAN_POINT ( 'NONE',  ( -16.50000000000000000, -20.00000000000000000, 1.084773659275596300E-61 ) ) ;
#1851=MANIFOLD_SOLID_BREP ( 'Imported1', #316 ) ;
#2002=AXIS2_PLACEMENT_3D ( 'NONE', #20195, #3925, #22310 ) ;
#2077=AXIS2_PLACEMENT_3D ( 'NONE', #11052, #8481, #9264 ) ;
#2105=DIRECTION ( 'NONE',  ( 3.099353312215989243E-62, -1.534091707905539548E-92, -1.000000000000000000 ) ) ;
#2132=DIRECTION ( 'NONE',  ( -1.000000000000000000, 0.000000000000000000, -3.099353312215991402E-62 ) ) ;
#2255=CYLINDRICAL_SURFACE ( 'NONE', #20918, 3.499999999999999556 ) ;
#2268=CARTESIAN_POINT ( 'NONE',  ( -20.00000000000000000, -20.00000000000000000, 5.000000000000000000 ) ) ;
#2292=DIRECTION ( 'NONE',  ( -1.000000000000000000, 0.000000000000000000, -3.099353312215989675E-62 ) ) ;
#2335=VERTEX_POINT ( 'NONE', #1718 ) ;
#2400=DIRECTION ( 'NONE',  ( -1.000000000000000000, 0.000000000000000000, 0.000000000000000000 ) ) ;
#2433=DIRECTION ( 'NONE',  ( 3.099353312215989243E-62, -1.534091707905539548E-92, -1.000000000000000000 ) ) ;
#2485=VERTEX_POINT ( 'NONE', #19901 ) ;
#2569=CARTESIAN_POINT ( 'NONE',  ( 0.000000000000000000, 0.000000000000000000, 0.000000000000000000 ) ) ;
#2683=( NAMED_UNIT ( * ) PLANE_ANGLE_UNIT ( ) SI_UNIT ( $, .RADIAN. ) );
#2801=VERTEX_POINT ( 'NONE', #8714 ) ;
#2860=DIRECTION ( 'NONE',  ( -1.000000000000000000, 0.000000000000000000, 0.000000000000000000 ) ) ;
#3257=ADVANCED_FACE ( 'NONE', ( #15780, #23007 ), #3304, .F. ) ;
#3258=EDGE_LOOP ( 'NONE', ( #3452, #11458 ) ) ;
#3304=PLANE ( 'NONE',  #15819 ) ;
#3446=EDGE_LOOP ( 'NONE', ( #3885, #22914, #20549, #15372 ) ) ;
#3452=ORIENTED_EDGE ( 'NONE', *, *, #6794, .F. ) ;
#3556=VERTEX_POINT ( 'NONE', #22627 ) ;
#3658=EDGE_LOOP ( 'NONE', ( #22201, #7290, #1293, #703 ) ) ;
#3885=ORIENTED_EDGE ( 'NONE', *, *, #15434, .F. ) ;
#3925=DIRECTION ( 'NONE',  ( -3.099353312215989243E-62, 1.534091707905539548E-92, 1.000000000000000000 ) ) ;
#4177=AXIS2_PLACEMENT_3D ( 'NONE', #23301, #8947, #135 ) ;
#4284=ORIENTED_EDGE ( 'NONE', *, *, #8922, .F. ) ;
#4390=ORIENTED_EDGE ( 'NONE', *, *, #22885, .T. ) ;
#4745=VERTEX_POINT ( 'NONE', #1316 ) ;
#4826=LINE ( 'NONE', #6492, #11673 ) ;
#4934=EDGE_CURVE ( 'NONE', #17992, #341, #22739, .T. ) ;
#4971=EDGE_LOOP ( 'NONE', ( #20897, #10976 ) ) ;
#5039=CARTESIAN_POINT ( 'NONE',  ( -20.00000000000000000, -20.00000000000000000, 0.000000000000000000 ) ) ;
#5278=LINE ( 'NONE', #14424, #21763 ) ;
#5829=VERTEX_POINT ( 'NONE', #8610 ) ;
#5893=PRODUCT_DEFINITION ( 'UNKNOWN', '', #14124, #10898 ) ;
#6233=VECTOR ( 'NONE', #19426, 1000.000000000000000 ) ;
#6254=SHAPE_REPRESENTATION_RELATIONSHIP ( 'NONE' , 'NONE' ,  #7037, #13910 ) ;
#6368=CIRCLE ( 'NONE', #11329, 3.499999999999999556 ) ;
#6492=CARTESIAN_POINT ( 'NONE',  ( -23.50000000000000000, -20.00000000000000000, 2.500000000000000000 ) ) ;
#6767=DIRECTION ( 'NONE',  ( 0.000000000000000000, -1.000000000000000000, 1.534091707905539548E-92 ) ) ;
#6794=EDGE_CURVE ( 'NONE', #5829, #4745, #12260, .T. ) ;
#6824=ORIENTED_EDGE ( 'NONE', *, *, #16581, .F. ) ;
#7037=SHAPE_REPRESENTATION ( '1602p_c_04', ( #12739 ), #7801 ) ;
#7148=CIRCLE ( 'NONE', #20413, 2.499999999999998668 ) ;
#7290=ORIENTED_EDGE ( 'NONE', *, *, #8922, .T. ) ;
#7395=FACE_OUTER_BOUND ( 'NONE', #15901, .T. ) ;
#7439=ORIENTED_EDGE ( 'NONE', *, *, #6794, .T. ) ;
#7484=CIRCLE ( 'NONE', #11678, 3.499999999999999556 ) ;
#7532=ADVANCED_FACE ( 'NONE', ( #11477 ), #12999, .F. ) ;
#7679=ORIENTED_EDGE ( 'NONE', *, *, #8835, .T. ) ;
#7754=ORIENTED_EDGE ( 'NONE', *, *, #16581, .T. ) ;
#7801=( GEOMETRIC_REPRESENTATION_CONTEXT ( 3 ) GLOBAL_UNCERTAINTY_ASSIGNED_CONTEXT ( ( #15284 ) ) GLOBAL_UNIT_ASSIGNED_CONTEXT ( ( #8516, #2683, #13497 ) ) REPRESENTATION_CONTEXT ( 'NONE', 'WORKASPACE' ) );
#7843=CARTESIAN_POINT ( 'NONE',  ( -20.00000000000000000, -20.00000000000000000, 0.000000000000000000 ) ) ;
#8202=CARTESIAN_POINT ( 'NONE',  ( -20.00000000000000000, -20.00000000000000000, 5.000000000000000000 ) ) ;
#8294=MECHANICAL_CONTEXT ( 'NONE', #20803, 'mechanical' ) ;
#8365=DIRECTION ( 'NONE',  ( 0.000000000000000000, -1.000000000000000000, 1.534091707905539548E-92 ) ) ;
#8419=VECTOR ( 'NONE', #1394, 1000.000000000000000 ) ;
#8429=CARTESIAN_POINT ( 'NONE',  ( -22.50000000000000000, -20.00000000000000000, -7.748383280539974188E-62 ) ) ;
#8481=DIRECTION ( 'NONE',  ( 3.099353312215989243E-62, -1.534091707905539548E-92, -1.000000000000000000 ) ) ;
#8516=( LENGTH_UNIT ( ) NAMED_UNIT ( * ) SI_UNIT ( .MILLI., .METRE. ) );
#8605=FACE_BOUND ( 'NONE', #460, .T. ) ;
#8610=CARTESIAN_POINT ( 'NONE',  ( -23.50000000000000000, -20.00000000000000000, 5.000000000000000000 ) ) ;
#8714=CARTESIAN_POINT ( 'NONE',  ( -17.50000000000000000, -20.00000000000000000, 5.000000000000000000 ) ) ;
#8835=EDGE_CURVE ( 'NONE', #3556, #17992, #13853, .T. ) ;
#8922=EDGE_CURVE ( 'NONE', #2801, #341, #5278, .T. ) ;
#8947=DIRECTION ( 'NONE',  ( 3.099353312215989243E-62, -1.534091707905539548E-92, -1.000000000000000000 ) ) ;
#9226=AXIS2_PLACEMENT_3D ( 'NONE', #15005, #2433, #13352 ) ;
#9264=DIRECTION ( 'NONE',  ( -1.000000000000000000, 0.000000000000000000, 0.000000000000000000 ) ) ;
#9284=DIRECTION ( 'NONE',  ( 3.099353312215989243E-62, -1.534091707905539548E-92, -1.000000000000000000 ) ) ;
#9383=ADVANCED_FACE ( 'NONE', ( #16071 ), #23413, .F. ) ;
#9517=CARTESIAN_POINT ( 'NONE',  ( -20.00000000000000000, -20.00000000000000000, 2.500000000000000000 ) ) ;
#9554=CARTESIAN_POINT ( 'NONE',  ( -20.00000000000000000, -20.00000000000000000, 0.000000000000000000 ) ) ;
#10153=DIRECTION ( 'NONE',  ( 3.099353312215989243E-62, -1.534091707905539548E-92, -1.000000000000000000 ) ) ;
#10662=ORIENTED_EDGE ( 'NONE', *, *, #4934, .T. ) ;
#10800=SHAPE_DEFINITION_REPRESENTATION ( #20879, #7037 ) ;
#10898=DESIGN_CONTEXT ( 'detailed design', #22956, 'design' ) ;
#10976=ORIENTED_EDGE ( 'NONE', *, *, #1217, .F. ) ;
#11052=CARTESIAN_POINT ( 'NONE',  ( -20.00000000000000000, -20.00000000000000000, 5.000000000000000000 ) ) ;
#11177=EDGE_LOOP ( 'NONE', ( #16121, #4390 ) ) ;
#11329=AXIS2_PLACEMENT_3D ( 'NONE', #13498, #22383, #765 ) ;
#11458=ORIENTED_EDGE ( 'NONE', *, *, #18221, .F. ) ;
#11477=FACE_OUTER_BOUND ( 'NONE', #20645, .T. ) ;
#11673=VECTOR ( 'NONE', #12433, 1000.000000000000000 ) ;
#11678=AXIS2_PLACEMENT_3D ( 'NONE', #9554, #20348, #2292 ) ;
#11949=CYLINDRICAL_SURFACE ( 'NONE', #12080, 3.499999999999999556 ) ;
#11986=EDGE_CURVE ( 'NONE', #2485, #2335, #6368, .T. ) ;
#12080=AXIS2_PLACEMENT_3D ( 'NONE', #15240, #10153, #19280 ) ;
#12260=CIRCLE ( 'NONE', #85, 3.499999999999999556 ) ;
#12433=DIRECTION ( 'NONE',  ( 3.099353312215988811E-62, -1.534091707905539548E-92, -1.000000000000000000 ) ) ;
#12739=AXIS2_PLACEMENT_3D ( 'NONE', #2569, #13380, #415 ) ;
#12999=CYLINDRICAL_SURFACE ( 'NONE', #9226, 2.499999999999998668 ) ;
#13015=EDGE_CURVE ( 'NONE', #3556, #2801, #7148, .T. ) ;
#13282=AXIS2_PLACEMENT_3D ( 'NONE', #7843, #21955, #2132 ) ;
#13352=DIRECTION ( 'NONE',  ( -1.000000000000000000, 0.000000000000000000, 0.000000000000000000 ) ) ;
#13380=DIRECTION ( 'NONE',  ( 0.000000000000000000, 0.000000000000000000, 1.000000000000000000 ) ) ;
#13497=( NAMED_UNIT ( * ) SI_UNIT ( $, .STERADIAN. ) SOLID_ANGLE_UNIT ( ) );
#13498=CARTESIAN_POINT ( 'NONE',  ( -20.00000000000000000, -20.00000000000000000, 0.000000000000000000 ) ) ;
#13676=ORIENTED_EDGE ( 'NONE', *, *, #13015, .F. ) ;
#13853=LINE ( 'NONE', #22738, #6233 ) ;
#13910=ADVANCED_BREP_SHAPE_REPRESENTATION ( '', ( #1851, #12739 ), #7801 ) ;
#14124=PRODUCT_DEFINITION_FORMATION_WITH_SPECIFIED_SOURCE ( 'ANY', '', #14605, .NOT_KNOWN. ) ;
#14348=CARTESIAN_POINT ( 'NONE',  ( -16.50000000000000000, -20.00000000000000000, 2.500000000000000000 ) ) ;
#14424=CARTESIAN_POINT ( 'NONE',  ( -17.50000000000000000, -20.00000000000000000, 2.500000000000000000 ) ) ;
#14605=PRODUCT ( '1602p_c_04', '1602p_c_04', '', ( #8294 ) ) ;
#15005=CARTESIAN_POINT ( 'NONE',  ( -20.00000000000000000, -20.00000000000000000, 2.500000000000000000 ) ) ;
#15240=CARTESIAN_POINT ( 'NONE',  ( -20.00000000000000000, -20.00000000000000000, 2.500000000000000000 ) ) ;
#15284=UNCERTAINTY_MEASURE_WITH_UNIT (LENGTH_MEASURE( 1.000000000000000082E-05 ), #8516, 'distance_accuracy_value', 'NONE');
#15372=ORIENTED_EDGE ( 'NONE', *, *, #11986, .T. ) ;
#15434=EDGE_CURVE ( 'NONE', #4745, #2335, #15888, .T. ) ;
#15667=CARTESIAN_POINT ( 'NONE',  ( -20.00000000000000000, -20.00000000000000000, 5.000000000000000000 ) ) ;
#15780=FACE_BOUND ( 'NONE', #11177, .T. ) ;
#15819=AXIS2_PLACEMENT_3D ( 'NONE', #15667, #21467, #6767 ) ;
#15888=LINE ( 'NONE', #14348, #8419 ) ;
#15891=ADVANCED_FACE ( 'NONE', ( #8605, #17397 ), #15952, .T. ) ;
#15901=EDGE_LOOP ( 'NONE', ( #7439, #297, #20617, #19137 ) ) ;
#15952=PLANE ( 'NONE',  #23198 ) ;
#16071=FACE_OUTER_BOUND ( 'NONE', #3658, .T. ) ;
#16121=ORIENTED_EDGE ( 'NONE', *, *, #13015, .T. ) ;
#16247=CARTESIAN_POINT ( 'NONE',  ( -20.00000000000000000, -20.00000000000000000, 5.000000000000000000 ) ) ;
#16509=DIRECTION ( 'NONE',  ( -1.000000000000000000, 0.000000000000000000, 0.000000000000000000 ) ) ;
#16581=EDGE_CURVE ( 'NONE', #341, #17992, #21727, .T. ) ;
#17397=FACE_OUTER_BOUND ( 'NONE', #4971, .T. ) ;
#17544=AXIS2_PLACEMENT_3D ( 'NONE', #16247, #2105, #308 ) ;
#17992=VERTEX_POINT ( 'NONE', #8429 ) ;
#18221=EDGE_CURVE ( 'NONE', #4745, #5829, #21003, .T. ) ;
#18408=CIRCLE ( 'NONE', #2077, 2.499999999999998668 ) ;
#18679=DIRECTION ( 'NONE',  ( 3.099353312215989243E-62, -1.534091707905539548E-92, -1.000000000000000000 ) ) ;
#19137=ORIENTED_EDGE ( 'NONE', *, *, #21862, .F. ) ;
#19280=DIRECTION ( 'NONE',  ( -1.000000000000000000, 0.000000000000000000, 0.000000000000000000 ) ) ;
#19426=DIRECTION ( 'NONE',  ( 3.099353312215988811E-62, -1.534091707905539548E-92, -1.000000000000000000 ) ) ;
#19901=CARTESIAN_POINT ( 'NONE',  ( -23.50000000000000000, -20.00000000000000000, -1.084773659275596300E-61 ) ) ;
#20195=CARTESIAN_POINT ( 'NONE',  ( -20.00000000000000000, -20.00000000000000000, 0.000000000000000000 ) ) ;
#20348=DIRECTION ( 'NONE',  ( -3.099353312215989243E-62, 1.534091707905539548E-92, 1.000000000000000000 ) ) ;
#20413=AXIS2_PLACEMENT_3D ( 'NONE', #2268, #18679, #2400 ) ;
#20549=ORIENTED_EDGE ( 'NONE', *, *, #21862, .T. ) ;
#20617=ORIENTED_EDGE ( 'NONE', *, *, #1217, .T. ) ;
#20645=EDGE_LOOP ( 'NONE', ( #4284, #13676, #7679, #6824 ) ) ;
#20803=APPLICATION_CONTEXT ( 'configuration controlled 3d designs of mechanical parts and assemblies' ) ;
#20879=PRODUCT_DEFINITION_SHAPE ( 'NONE', 'NONE',  #5893 ) ;
#20897=ORIENTED_EDGE ( 'NONE', *, *, #11986, .F. ) ;
#20918=AXIS2_PLACEMENT_3D ( 'NONE', #9517, #9284, #16509 ) ;
#21003=CIRCLE ( 'NONE', #17544, 3.499999999999999556 ) ;
#21467=DIRECTION ( 'NONE',  ( 3.099353312215988811E-62, -1.534091707905539548E-92, -1.000000000000000000 ) ) ;
#21727=CIRCLE ( 'NONE', #2002, 2.499999999999998668 ) ;
#21763=VECTOR ( 'NONE', #1716, 1000.000000000000000 ) ;
#21862=EDGE_CURVE ( 'NONE', #5829, #2485, #4826, .T. ) ;
#21955=DIRECTION ( 'NONE',  ( -3.099353312215989243E-62, 1.534091707905539548E-92, 1.000000000000000000 ) ) ;
#22201=ORIENTED_EDGE ( 'NONE', *, *, #22885, .F. ) ;
#22310=DIRECTION ( 'NONE',  ( -1.000000000000000000, 0.000000000000000000, -3.099353312215991402E-62 ) ) ;
#22383=DIRECTION ( 'NONE',  ( -3.099353312215989243E-62, 1.534091707905539548E-92, 1.000000000000000000 ) ) ;
#22627=CARTESIAN_POINT ( 'NONE',  ( -22.50000000000000000, -20.00000000000000000, 5.000000000000000000 ) ) ;
#22670=DIRECTION ( 'NONE',  ( 3.099353312215989243E-62, -1.534091707905539548E-92, -1.000000000000000000 ) ) ;
#22716=ADVANCED_FACE ( 'NONE', ( #732 ), #11949, .T. ) ;
#22738=CARTESIAN_POINT ( 'NONE',  ( -22.50000000000000000, -20.00000000000000000, 2.500000000000000000 ) ) ;
#22739=CIRCLE ( 'NONE', #13282, 2.499999999999998668 ) ;
#22760=CARTESIAN_POINT ( 'NONE',  ( -17.50000000000000000, -20.00000000000000000, 7.748383280539972460E-62 ) ) ;
#22885=EDGE_CURVE ( 'NONE', #2801, #3556, #18408, .T. ) ;
#22914=ORIENTED_EDGE ( 'NONE', *, *, #18221, .T. ) ;
#22956=APPLICATION_CONTEXT ( 'configuration controlled 3d designs of mechanical parts and assemblies' ) ;
#23007=FACE_OUTER_BOUND ( 'NONE', #3258, .T. ) ;
#23198=AXIS2_PLACEMENT_3D ( 'NONE', #5039, #987, #8365 ) ;
#23301=CARTESIAN_POINT ( 'NONE',  ( -20.00000000000000000, -20.00000000000000000, 2.500000000000000000 ) ) ;
#23413=CYLINDRICAL_SURFACE ( 'NONE', #4177, 2.499999999999998668 ) ;
#23522=COLOUR_RGB('Light Blue', 0.66274510, 0.83137255, 0.94901961);
#23523=FILL_AREA_STYLE_COLOUR('',#23522);
#23524=FILL_AREA_STYLE('',(#23523));
#23525=SURFACE_STYLE_FILL_AREA(#23524);
#23526=SURFACE_SIDE_STYLE('',(#23525));
#23527=SURFACE_STYLE_USAGE(.BOTH.,#23526);
#23528=PRESENTATION_STYLE_ASSIGNMENT((#23527));
#23599=STYLED_ITEM('',(#23528),#1851);
#23600=MECHANICAL_DESIGN_GEOMETRIC_PRESENTATION_REPRESENTATION('',(#23599),#7801);
ENDSEC;
END-ISO-10303-21;
